ISO-10303-21;
HEADER;
/* Generated by software containing ST-Developer
 * from STEP Tools, Inc. (www.steptools.com) 
 */

FILE_DESCRIPTION(
/* description */ ('PAT-015'),
/* implementation_level */ '2;1');

FILE_NAME(
/* name */ 'Socket Set Screw - M4x6.step',
/* time_stamp */ '2026-10-29T16:03:43-07:00',
/* author */ (''),
/* organization */ (''),
/* preprocessor_version */ 'ST-DEVELOPER v20.2',
/* originating_system */ 'Autodesk Translation Framework v15.17.0.0',
/* authorisation */ '');

FILE_SCHEMA (('AUTOMOTIVE_DESIGN { 1 0 10303 214 3 1 1 }'));
ENDSEC;

DATA;
#10=MECHANICAL_DESIGN_GEOMETRIC_PRESENTATION_REPRESENTATION('',(#251),#10266);
#176=CONICAL_SURFACE('',#5474,0.185,0.785398163397449);
#177=CONICAL_SURFACE('',#5478,0.1625,0.785398163397449);
#203=SHAPE_REPRESENTATION_RELATIONSHIP('SRR','None',#10374,#226);
#226=ADVANCED_BREP_SHAPE_REPRESENTATION('',(#275),#10262);
#251=STYLED_ITEM('',(#10554),#275);
#275=MANIFOLD_SOLID_BREP('Body1',#4711);
#416=FACE_BOUND('',#1232,.T.);
#545=PLANE('',#5465);
#546=PLANE('',#5466);
#547=PLANE('',#5467);
#548=PLANE('',#5468);
#549=PLANE('',#5469);
#550=PLANE('',#5470);
#551=PLANE('',#5471);
#552=PLANE('',#5472);
#553=PLANE('',#5480);
#817=FACE_OUTER_BOUND('',#1224,.T.);
#818=FACE_OUTER_BOUND('',#1225,.T.);
#819=FACE_OUTER_BOUND('',#1226,.T.);
#820=FACE_OUTER_BOUND('',#1227,.T.);
#821=FACE_OUTER_BOUND('',#1228,.T.);
#822=FACE_OUTER_BOUND('',#1229,.T.);
#823=FACE_OUTER_BOUND('',#1230,.T.);
#824=FACE_OUTER_BOUND('',#1231,.T.);
#825=FACE_OUTER_BOUND('',#1233,.T.);
#826=FACE_OUTER_BOUND('',#1234,.T.);
#827=FACE_OUTER_BOUND('',#1235,.T.);
#828=FACE_OUTER_BOUND('',#1236,.T.);
#1224=EDGE_LOOP('',(#4143,#4144,#4145,#4146));
#1225=EDGE_LOOP('',(#4147,#4148,#4149,#4150));
#1226=EDGE_LOOP('',(#4151,#4152,#4153,#4154));
#1227=EDGE_LOOP('',(#4155,#4156,#4157,#4158));
#1228=EDGE_LOOP('',(#4159,#4160,#4161,#4162));
#1229=EDGE_LOOP('',(#4163,#4164,#4165,#4166));
#1230=EDGE_LOOP('',(#4167,#4168,#4169,#4170,#4171,#4172));
#1231=EDGE_LOOP('',(#4173));
#1232=EDGE_LOOP('',(#4174,#4175,#4176,#4177,#4178,#4179));
#1233=EDGE_LOOP('',(#4180,#4181,#4182,#4183));
#1234=EDGE_LOOP('',(#4184,#4185,#4186,#4187));
#1235=EDGE_LOOP('',(#4188,#4189,#4190,#4191));
#1236=EDGE_LOOP('',(#4192));
#1545=LINE('',#10024,#1825);
#1546=LINE('',#10026,#1826);
#1547=LINE('',#10028,#1827);
#1548=LINE('',#10029,#1828);
#1549=LINE('',#10032,#1829);
#1550=LINE('',#10034,#1830);
#1551=LINE('',#10035,#1831);
#1552=LINE('',#10038,#1832);
#1553=LINE('',#10040,#1833);
#1554=LINE('',#10041,#1834);
#1555=LINE('',#10044,#1835);
#1556=LINE('',#10046,#1836);
#1557=LINE('',#10047,#1837);
#1558=LINE('',#10050,#1838);
#1559=LINE('',#10052,#1839);
#1560=LINE('',#10053,#1840);
#1561=LINE('',#10055,#1841);
#1562=LINE('',#10056,#1842);
#1563=LINE('',#10064,#1843);
#1564=LINE('',#10068,#1844);
#1565=LINE('',#10072,#1845);
#1825=VECTOR('',#6770,1.);
#1826=VECTOR('',#6771,1.);
#1827=VECTOR('',#6772,1.);
#1828=VECTOR('',#6773,1.);
#1829=VECTOR('',#6776,1.);
#1830=VECTOR('',#6777,1.);
#1831=VECTOR('',#6778,1.);
#1832=VECTOR('',#6781,1.);
#1833=VECTOR('',#6782,1.);
#1834=VECTOR('',#6783,1.);
#1835=VECTOR('',#6786,1.);
#1836=VECTOR('',#6787,1.);
#1837=VECTOR('',#6788,1.);
#1838=VECTOR('',#6791,1.);
#1839=VECTOR('',#6792,1.);
#1840=VECTOR('',#6793,1.);
#1841=VECTOR('',#6796,1.);
#1842=VECTOR('',#6797,1.);
#1843=VECTOR('',#6808,0.185);
#1844=VECTOR('',#6813,0.2);
#1845=VECTOR('',#6818,0.1625);
#2098=CIRCLE('',#5473,0.17);
#2099=CIRCLE('',#5475,0.1954);
#2100=CIRCLE('',#5477,0.1954);
#2101=CIRCLE('',#5479,0.125);
#2459=VERTEX_POINT('',#10022);
#2460=VERTEX_POINT('',#10023);
#2461=VERTEX_POINT('',#10025);
#2462=VERTEX_POINT('',#10027);
#2463=VERTEX_POINT('',#10031);
#2464=VERTEX_POINT('',#10033);
#2465=VERTEX_POINT('',#10037);
#2466=VERTEX_POINT('',#10039);
#2467=VERTEX_POINT('',#10043);
#2468=VERTEX_POINT('',#10045);
#2469=VERTEX_POINT('',#10049);
#2470=VERTEX_POINT('',#10051);
#2471=VERTEX_POINT('',#10059);
#2472=VERTEX_POINT('',#10062);
#2473=VERTEX_POINT('',#10066);
#2474=VERTEX_POINT('',#10070);
#3027=EDGE_CURVE('',#2459,#2460,#1545,.T.);
#3028=EDGE_CURVE('',#2459,#2461,#1546,.T.);
#3029=EDGE_CURVE('',#2461,#2462,#1547,.T.);
#3030=EDGE_CURVE('',#2460,#2462,#1548,.T.);
#3031=EDGE_CURVE('',#2463,#2459,#1549,.T.);
#3032=EDGE_CURVE('',#2463,#2464,#1550,.T.);
#3033=EDGE_CURVE('',#2464,#2461,#1551,.T.);
#3034=EDGE_CURVE('',#2465,#2463,#1552,.T.);
#3035=EDGE_CURVE('',#2465,#2466,#1553,.T.);
#3036=EDGE_CURVE('',#2466,#2464,#1554,.T.);
#3037=EDGE_CURVE('',#2467,#2465,#1555,.T.);
#3038=EDGE_CURVE('',#2467,#2468,#1556,.T.);
#3039=EDGE_CURVE('',#2468,#2466,#1557,.T.);
#3040=EDGE_CURVE('',#2469,#2467,#1558,.T.);
#3041=EDGE_CURVE('',#2469,#2470,#1559,.T.);
#3042=EDGE_CURVE('',#2470,#2468,#1560,.T.);
#3043=EDGE_CURVE('',#2460,#2469,#1561,.T.);
#3044=EDGE_CURVE('',#2462,#2470,#1562,.T.);
#3045=EDGE_CURVE('',#2471,#2471,#2098,.T.);
#3046=EDGE_CURVE('',#2472,#2472,#2099,.T.);
#3047=EDGE_CURVE('',#2472,#2471,#1563,.T.);
#3048=EDGE_CURVE('',#2473,#2473,#2100,.F.);
#3049=EDGE_CURVE('',#2473,#2472,#1564,.T.);
#3050=EDGE_CURVE('',#2474,#2474,#2101,.T.);
#3051=EDGE_CURVE('',#2474,#2473,#1565,.T.);
#4143=ORIENTED_EDGE('',*,*,#3027,.F.);
#4144=ORIENTED_EDGE('',*,*,#3028,.T.);
#4145=ORIENTED_EDGE('',*,*,#3029,.T.);
#4146=ORIENTED_EDGE('',*,*,#3030,.F.);
#4147=ORIENTED_EDGE('',*,*,#3031,.F.);
#4148=ORIENTED_EDGE('',*,*,#3032,.T.);
#4149=ORIENTED_EDGE('',*,*,#3033,.T.);
#4150=ORIENTED_EDGE('',*,*,#3028,.F.);
#4151=ORIENTED_EDGE('',*,*,#3034,.F.);
#4152=ORIENTED_EDGE('',*,*,#3035,.T.);
#4153=ORIENTED_EDGE('',*,*,#3036,.T.);
#4154=ORIENTED_EDGE('',*,*,#3032,.F.);
#4155=ORIENTED_EDGE('',*,*,#3037,.F.);
#4156=ORIENTED_EDGE('',*,*,#3038,.T.);
#4157=ORIENTED_EDGE('',*,*,#3039,.T.);
#4158=ORIENTED_EDGE('',*,*,#3035,.F.);
#4159=ORIENTED_EDGE('',*,*,#3040,.F.);
#4160=ORIENTED_EDGE('',*,*,#3041,.T.);
#4161=ORIENTED_EDGE('',*,*,#3042,.T.);
#4162=ORIENTED_EDGE('',*,*,#3038,.F.);
#4163=ORIENTED_EDGE('',*,*,#3043,.F.);
#4164=ORIENTED_EDGE('',*,*,#3030,.T.);
#4165=ORIENTED_EDGE('',*,*,#3044,.T.);
#4166=ORIENTED_EDGE('',*,*,#3041,.F.);
#4167=ORIENTED_EDGE('',*,*,#3044,.F.);
#4168=ORIENTED_EDGE('',*,*,#3029,.F.);
#4169=ORIENTED_EDGE('',*,*,#3033,.F.);
#4170=ORIENTED_EDGE('',*,*,#3036,.F.);
#4171=ORIENTED_EDGE('',*,*,#3039,.F.);
#4172=ORIENTED_EDGE('',*,*,#3042,.F.);
#4173=ORIENTED_EDGE('',*,*,#3045,.F.);
#4174=ORIENTED_EDGE('',*,*,#3027,.T.);
#4175=ORIENTED_EDGE('',*,*,#3043,.T.);
#4176=ORIENTED_EDGE('',*,*,#3040,.T.);
#4177=ORIENTED_EDGE('',*,*,#3037,.T.);
#4178=ORIENTED_EDGE('',*,*,#3034,.T.);
#4179=ORIENTED_EDGE('',*,*,#3031,.T.);
#4180=ORIENTED_EDGE('',*,*,#3046,.F.);
#4181=ORIENTED_EDGE('',*,*,#3047,.T.);
#4182=ORIENTED_EDGE('',*,*,#3045,.T.);
#4183=ORIENTED_EDGE('',*,*,#3047,.F.);
#4184=ORIENTED_EDGE('',*,*,#3048,.F.);
#4185=ORIENTED_EDGE('',*,*,#3049,.T.);
#4186=ORIENTED_EDGE('',*,*,#3046,.T.);
#4187=ORIENTED_EDGE('',*,*,#3049,.F.);
#4188=ORIENTED_EDGE('',*,*,#3050,.F.);
#4189=ORIENTED_EDGE('',*,*,#3051,.T.);
#4190=ORIENTED_EDGE('',*,*,#3048,.T.);
#4191=ORIENTED_EDGE('',*,*,#3051,.F.);
#4192=ORIENTED_EDGE('',*,*,#3050,.T.);
#4402=CYLINDRICAL_SURFACE('',#5476,0.1954);
#4652=ADVANCED_FACE('',(#817),#545,.F.);
#4653=ADVANCED_FACE('',(#818),#546,.F.);
#4654=ADVANCED_FACE('',(#819),#547,.F.);
#4655=ADVANCED_FACE('',(#820),#548,.F.);
#4656=ADVANCED_FACE('',(#821),#549,.F.);
#4657=ADVANCED_FACE('',(#822),#550,.F.);
#4658=ADVANCED_FACE('',(#823),#551,.F.);
#4659=ADVANCED_FACE('',(#824,#416),#552,.T.);
#4660=ADVANCED_FACE('',(#825),#176,.T.);
#4661=ADVANCED_FACE('',(#826),#4402,.T.);
#4662=ADVANCED_FACE('',(#827),#177,.T.);
#4663=ADVANCED_FACE('',(#828),#553,.T.);
#4711=CLOSED_SHELL('',(#4652,#4653,#4654,#4655,#4656,#4657,#4658,#4659,
#4660,#4661,#4662,#4663));
#5464=AXIS2_PLACEMENT_3D('',#10020,#6766,#6767);
#5465=AXIS2_PLACEMENT_3D('',#10021,#6768,#6769);
#5466=AXIS2_PLACEMENT_3D('',#10030,#6774,#6775);
#5467=AXIS2_PLACEMENT_3D('',#10036,#6779,#6780);
#5468=AXIS2_PLACEMENT_3D('',#10042,#6784,#6785);
#5469=AXIS2_PLACEMENT_3D('',#10048,#6789,#6790);
#5470=AXIS2_PLACEMENT_3D('',#10054,#6794,#6795);
#5471=AXIS2_PLACEMENT_3D('',#10057,#6798,#6799);
#5472=AXIS2_PLACEMENT_3D('',#10058,#6800,#6801);
#5473=AXIS2_PLACEMENT_3D('',#10060,#6802,#6803);
#5474=AXIS2_PLACEMENT_3D('',#10061,#6804,#6805);
#5475=AXIS2_PLACEMENT_3D('',#10063,#6806,#6807);
#5476=AXIS2_PLACEMENT_3D('',#10065,#6809,#6810);
#5477=AXIS2_PLACEMENT_3D('',#10067,#6811,#6812);
#5478=AXIS2_PLACEMENT_3D('',#10069,#6814,#6815);
#5479=AXIS2_PLACEMENT_3D('',#10071,#6816,#6817);
#5480=AXIS2_PLACEMENT_3D('',#10073,#6819,#6820);
#6766=DIRECTION('axis',(0.,0.,1.));
#6767=DIRECTION('refdir',(1.,0.,0.));
#6768=DIRECTION('center_axis',(0.866025403784439,0.,-0.5));
#6769=DIRECTION('ref_axis',(0.5,0.,0.866025403784439));
#6770=DIRECTION('',(0.5,0.,0.866025403784439));
#6771=DIRECTION('',(0.,-1.,0.));
#6772=DIRECTION('',(0.5,0.,0.866025403784439));
#6773=DIRECTION('',(0.,-1.,0.));
#6774=DIRECTION('center_axis',(1.20185167898973E-16,0.,-1.));
#6775=DIRECTION('ref_axis',(1.,0.,1.20185167898973E-16));
#6776=DIRECTION('',(1.,0.,1.20185167898973E-16));
#6777=DIRECTION('',(0.,-1.,0.));
#6778=DIRECTION('',(1.,0.,1.20185167898973E-16));
#6779=DIRECTION('center_axis',(-0.866025403784439,0.,-0.5));
#6780=DIRECTION('ref_axis',(0.5,0.,-0.866025403784439));
#6781=DIRECTION('',(0.5,0.,-0.866025403784439));
#6782=DIRECTION('',(0.,-1.,0.));
#6783=DIRECTION('',(0.5,0.,-0.866025403784439));
#6784=DIRECTION('center_axis',(-0.866025403784439,0.,0.5));
#6785=DIRECTION('ref_axis',(-0.5,0.,-0.866025403784439));
#6786=DIRECTION('',(-0.5,0.,-0.866025403784439));
#6787=DIRECTION('',(0.,-1.,0.));
#6788=DIRECTION('',(-0.5,0.,-0.866025403784439));
#6789=DIRECTION('center_axis',(-2.40370335797945E-16,0.,1.));
#6790=DIRECTION('ref_axis',(-1.,0.,-2.40370335797945E-16));
#6791=DIRECTION('',(-1.,0.,-2.40370335797945E-16));
#6792=DIRECTION('',(0.,-1.,0.));
#6793=DIRECTION('',(-1.,0.,-2.40370335797945E-16));
#6794=DIRECTION('center_axis',(0.866025403784439,0.,0.5));
#6795=DIRECTION('ref_axis',(-0.5,0.,0.866025403784439));
#6796=DIRECTION('',(-0.5,0.,0.866025403784439));
#6797=DIRECTION('',(-0.5,0.,0.866025403784439));
#6798=DIRECTION('center_axis',(0.,-1.,0.));
#6799=DIRECTION('ref_axis',(0.,0.,-1.));
#6800=DIRECTION('center_axis',(0.,1.,0.));
#6801=DIRECTION('ref_axis',(0.,0.,1.));
#6802=DIRECTION('center_axis',(0.,-1.,0.));
#6803=DIRECTION('ref_axis',(1.,0.,0.));
#6804=DIRECTION('center_axis',(0.,-1.,0.));
#6805=DIRECTION('ref_axis',(1.,0.,0.));
#6806=DIRECTION('center_axis',(0.,-1.,0.));
#6807=DIRECTION('ref_axis',(1.,0.,0.));
#6808=DIRECTION('',(0.707106781186548,0.707106781186547,8.65956056235494E-17));
#6809=DIRECTION('center_axis',(0.,-1.,0.));
#6810=DIRECTION('ref_axis',(1.,0.,0.));
#6811=DIRECTION('center_axis',(0.,1.,0.));
#6812=DIRECTION('ref_axis',(1.,0.,0.));
#6813=DIRECTION('',(0.,1.,0.));
#6814=DIRECTION('center_axis',(0.,1.,0.));
#6815=DIRECTION('ref_axis',(1.,0.,0.));
#6816=DIRECTION('center_axis',(0.,-1.,0.));
#6817=DIRECTION('ref_axis',(1.,0.,0.));
#6818=DIRECTION('',(-0.707106781186548,0.707106781186547,-8.65956056235494E-17));
#6819=DIRECTION('center_axis',(0.,-1.,0.));
#6820=DIRECTION('ref_axis',(0.,0.,-1.));
#10020=CARTESIAN_POINT('',(0.,0.,0.));
#10021=CARTESIAN_POINT('Origin',(0.0577350269189626,0.,-0.1));
#10022=CARTESIAN_POINT('',(0.0577350269189626,0.,-0.1));
#10023=CARTESIAN_POINT('',(0.115470053837925,0.,0.));
#10024=CARTESIAN_POINT('',(0.0934187836487032,0.,-0.0381939203391614));
#10025=CARTESIAN_POINT('',(0.0577350269189626,-0.2,-0.1));
#10026=CARTESIAN_POINT('',(0.0577350269189626,0.,-0.1));
#10027=CARTESIAN_POINT('',(0.115470053837925,-0.2,0.));
#10028=CARTESIAN_POINT('',(0.115470053837925,-0.2,0.));
#10029=CARTESIAN_POINT('',(0.115470053837925,0.,0.));
#10030=CARTESIAN_POINT('Origin',(-0.0577350269189626,0.,-0.1));
#10031=CARTESIAN_POINT('',(-0.0577350269189626,0.,-0.1));
#10032=CARTESIAN_POINT('',(0.0561324865405187,0.,-0.1));
#10033=CARTESIAN_POINT('',(-0.0577350269189626,-0.2,-0.1));
#10034=CARTESIAN_POINT('',(-0.0577350269189626,0.,-0.1));
#10035=CARTESIAN_POINT('',(0.0577350269189626,-0.2,-0.1));
#10036=CARTESIAN_POINT('Origin',(-0.115470053837925,0.,-1.38777878078145E-17));
#10037=CARTESIAN_POINT('',(-0.115470053837925,0.,-1.41410031829988E-17));
#10038=CARTESIAN_POINT('',(-0.0797862971081845,0.,-0.0618060796608387));
#10039=CARTESIAN_POINT('',(-0.115470053837925,-0.2,-1.38777878078145E-17));
#10040=CARTESIAN_POINT('',(-0.115470053837925,0.,-1.41410031829988E-17));
#10041=CARTESIAN_POINT('',(-0.0577350269189626,-0.2,-0.1));
#10042=CARTESIAN_POINT('Origin',(-0.0577350269189626,0.,0.1));
#10043=CARTESIAN_POINT('',(-0.0577350269189626,0.,0.1));
#10044=CARTESIAN_POINT('',(-0.0509187836487033,0.,0.111806079660839));
#10045=CARTESIAN_POINT('',(-0.0577350269189626,-0.2,0.1));
#10046=CARTESIAN_POINT('',(-0.0577350269189626,0.,0.1));
#10047=CARTESIAN_POINT('',(-0.115470053837925,-0.2,-1.41410031829988E-17));
#10048=CARTESIAN_POINT('Origin',(0.0577350269189626,0.,0.1));
#10049=CARTESIAN_POINT('',(0.0577350269189626,0.,0.1));
#10050=CARTESIAN_POINT('',(0.113867513459481,0.,0.1));
#10051=CARTESIAN_POINT('',(0.0577350269189626,-0.2,0.1));
#10052=CARTESIAN_POINT('',(0.0577350269189626,0.,0.1));
#10053=CARTESIAN_POINT('',(-0.0577350269189626,-0.2,0.1));
#10054=CARTESIAN_POINT('Origin',(0.115470053837925,0.,0.));
#10055=CARTESIAN_POINT('',(0.122286297108185,0.,-0.0118060796608386));
#10056=CARTESIAN_POINT('',(0.0577350269189626,-0.2,0.1));
#10057=CARTESIAN_POINT('Origin',(0.,-0.2,0.));
#10058=CARTESIAN_POINT('Origin',(0.17,0.,0.));
#10059=CARTESIAN_POINT('',(-0.17,-8.67361737988404E-18,-2.0818995585505E-17));
#10060=CARTESIAN_POINT('Origin',(0.,0.,0.));
#10061=CARTESIAN_POINT('Origin',(0.,-0.015,0.));
#10062=CARTESIAN_POINT('',(-0.1954,-0.0254,-2.39295984553393E-17));
#10063=CARTESIAN_POINT('Origin',(0.,-0.0254,0.));
#10064=CARTESIAN_POINT('',(-0.185,-0.015,-2.2655965784226E-17));
#10065=CARTESIAN_POINT('Origin',(0.,-0.2775,0.));
#10066=CARTESIAN_POINT('',(-0.1954,-0.5296,2.39295984553393E-17));
#10067=CARTESIAN_POINT('Origin',(0.,-0.5296,0.));
#10068=CARTESIAN_POINT('',(-0.1954,-0.2775,-2.39295984553393E-17));
#10069=CARTESIAN_POINT('Origin',(0.,-0.5625,0.));
#10070=CARTESIAN_POINT('',(-0.125,-0.6,-1.53080849893419E-17));
#10071=CARTESIAN_POINT('Origin',(0.,-0.6,0.));
#10072=CARTESIAN_POINT('',(-0.1625,-0.5625,-1.99005104861445E-17));
#10073=CARTESIAN_POINT('Origin',(0.,-0.6,0.));
#10237=UNCERTAINTY_MEASURE_WITH_UNIT(LENGTH_MEASURE(0.001),#10267,
'DISTANCE_ACCURACY_VALUE',
'Maximum model space distance between geometric entities at asserted c
onnectivities');
#10241=UNCERTAINTY_MEASURE_WITH_UNIT(LENGTH_MEASURE(0.001),#10267,
'DISTANCE_ACCURACY_VALUE',
'Maximum model space distance between geometric entities at asserted c
onnectivities');
#10262=(
GEOMETRIC_REPRESENTATION_CONTEXT(3)
GLOBAL_UNCERTAINTY_ASSIGNED_CONTEXT((#10237))
GLOBAL_UNIT_ASSIGNED_CONTEXT((#10267,#10269,#10270))
REPRESENTATION_CONTEXT('','3D')
);
#10266=(
GEOMETRIC_REPRESENTATION_CONTEXT(3)
GLOBAL_UNCERTAINTY_ASSIGNED_CONTEXT((#10241))
GLOBAL_UNIT_ASSIGNED_CONTEXT((#10267,#10269,#10270))
REPRESENTATION_CONTEXT('','3D')
);
#10267=(
LENGTH_UNIT()
NAMED_UNIT(*)
SI_UNIT(.CENTI.,.METRE.)
);
#10269=(
NAMED_UNIT(*)
PLANE_ANGLE_UNIT()
SI_UNIT($,.RADIAN.)
);
#10270=(
NAMED_UNIT(*)
SI_UNIT($,.STERADIAN.)
SOLID_ANGLE_UNIT()
);
#10291=SHAPE_DEFINITION_REPRESENTATION(#10315,#10374);
#10315=PRODUCT_DEFINITION_SHAPE('',$,#10399);
#10374=SHAPE_REPRESENTATION('',(#5464),#10262);
#10378=PRODUCT_DEFINITION_CONTEXT('part definition',#10452,'design');
#10399=PRODUCT_DEFINITION('Socket Set Screw - M4x6',
'Socket Set Screw - M4x6',#10423,#10378);
#10423=PRODUCT_DEFINITION_FORMATION('',$,#10474);
#10452=APPLICATION_CONTEXT(
'Core Data for Automotive Mechanical Design Process');
#10453=PRODUCT_CONTEXT('part definition',#10452,'mechanical');
#10474=PRODUCT('Socket Set Screw - M4x6','Socket Set Screw - M4x6',
'Socket Set Screw - M4x6',(#10453));
#10548=COLOUR_RGB('Black',0.12,0.14,0.17);
#10549=FILL_AREA_STYLE_COLOUR('',#10548);
#10550=FILL_AREA_STYLE('',(#10549));
#10551=SURFACE_STYLE_FILL_AREA(#10550);
#10552=SURFACE_SIDE_STYLE('',(#10551));
#10553=SURFACE_STYLE_USAGE(.BOTH.,#10552);
#10554=PRESENTATION_STYLE_ASSIGNMENT((#10553));
ENDSEC;
END-ISO-10303-21;
